ISO-10303-21;
HEADER;
FILE_DESCRIPTION (('STEP AP214'),
    '1' );
FILE_NAME ('socket head cap screw_iso_ISO 4762 M3 x 8 - 8N.step',
    '2026-10-08T12:12:07',
    ( '' ),
    ( '' ),
    'SwSTEP 2.0',
    'SolidWorks 2026',
    '' );
FILE_SCHEMA (( 'AUTOMOTIVE_DESIGN' ));
ENDSEC;

DATA;
#1=ORIENTED_EDGE ( 'NONE', *, *, #482, .T. ) ;
#3=ORIENTED_EDGE ( 'NONE', *, *, #6998, .T. ) ;
#8=CARTESIAN_POINT ( 'NONE',  ( 11.00000000000000355, 0.000000000000000000, 1.219500000000000028 ) ) ;
#9=ADVANCED_BREP_SHAPE_REPRESENTATION ( '', ( #3934, #1587 ), #3111 ) ;
#13=ORIENTED_EDGE ( 'NONE', *, *, #1918, .T. ) ;
#24=ADVANCED_FACE ( 'NONE', ( #2123 ), #1462, .F. ) ;
#28=CARTESIAN_POINT ( 'NONE',  ( 1.300000000000000044, 1.478016689125442484, -1.626303258728256651E-15 ) ) ;
#39=ORIENTED_EDGE ( 'NONE', *, *, #6953, .F. ) ;
#60=EDGE_CURVE ( 'NONE', #480, #1132, #5248, .T. ) ;
#84=EDGE_CURVE ( 'NONE', #954, #5289, #7760, .T. ) ;
#96=ADVANCED_FACE ( 'NONE', ( #5364 ), #2158, .T. ) ;
#119=ORIENTED_EDGE ( 'NONE', *, *, #7559, .F. ) ;
#148=EDGE_CURVE ( 'NONE', #2318, #1485, #8001, .T. ) ;
#178=CARTESIAN_POINT ( 'NONE',  ( 3.099999999999998757, 1.836970198721030181E-16, -1.500000000000000222 ) ) ;
#183=LINE ( 'NONE', #4716, #4981 ) ;
#198=ORIENTED_EDGE ( 'NONE', *, *, #4864, .T. ) ;
#207=ORIENTED_EDGE ( 'NONE', *, *, #7666, .F. ) ;
#228=EDGE_LOOP ( 'NONE', ( #2747, #2923, #3072 ) ) ;
#230=AXIS2_PLACEMENT_3D ( 'NONE', #1621, #2735, #4150 ) ;
#233=CARTESIAN_POINT ( 'NONE',  ( -31.74999999999995737, 0.000000000000000000, 0.000000000000000000 ) ) ;
#243=ORIENTED_EDGE ( 'NONE', *, *, #3460, .F. ) ;
#254=DIRECTION ( 'NONE',  ( -1.000000000000000000, -0.000000000000000000, -0.000000000000000000 ) ) ;
#260=ORIENTED_EDGE ( 'NONE', *, *, #7666, .T. ) ;
#268=CARTESIAN_POINT ( 'NONE',  ( 0.000000000000000000, 3.275930187719169848E-16, -2.600000000000000089 ) ) ;
#269=ORIENTED_EDGE ( 'NONE', *, *, #5618, .F. ) ;
#274=CARTESIAN_POINT ( 'NONE',  ( 0.000000000000000000, 1.478016689125442484, -1.626303258728256651E-15 ) ) ;
#279=DIRECTION ( 'NONE',  ( 0.000000000000000000, 0.8660254037844380415, -0.5000000000000009992 ) ) ;
#280=SHAPE_DEFINITION_REPRESENTATION ( #4248, #3059 ) ;
#301=EDGE_LOOP ( 'NONE', ( #243, #2979, #6327, #8103 ) ) ;
#307=DIRECTION ( 'NONE',  ( 0.000000000000000000, 1.000000000000000000, -1.320393690296331133E-15 ) ) ;
#320=SURFACE_SIDE_STYLE ('',( #905 ) ) ;
#324=CARTESIAN_POINT ( 'NONE',  ( 1.300000000000000044, 1.690103923579304181E-15, 1.280000000000000249 ) ) ;
#328=SHAPE_REPRESENTATION_RELATIONSHIP ( 'NONE' , 'NONE' ,  #3059, #9 ) ;
#355=VECTOR ( 'NONE', #5353, 1000.000000000000114 ) ;
#383=UNCERTAINTY_MEASURE_WITH_UNIT (LENGTH_MEASURE( 1.000000000000000082E-05 ), #5531, 'distance_accuracy_value', 'NONE');
#384=AXIS2_PLACEMENT_3D ( 'NONE', #6730, #6116, #6907 ) ;
#409=( NAMED_UNIT ( * ) SI_UNIT ( $, .STERADIAN. ) SOLID_ANGLE_UNIT ( ) );
#415=CARTESIAN_POINT ( 'NONE',  ( -31.74999999999995737, 3.367778697655221012E-16, -2.750000000000000000 ) ) ;
#433=LINE ( 'NONE', #7335, #3573 ) ;
#435=CARTESIAN_POINT ( 'NONE',  ( 1.300000000000000044, 0.7390083445627193548, -1.280000000000000693 ) ) ;
#472=ORIENTED_EDGE ( 'NONE', *, *, #697, .T. ) ;
#473=VECTOR ( 'NONE', #2777, 1000.000000000000000 ) ;
#474=DIRECTION ( 'NONE',  ( 0.000000000000000000, 0.000000000000000000, 1.000000000000000000 ) ) ;
#475=CARTESIAN_POINT ( 'NONE',  ( 3.099999999999998757, 0.000000000000000000, -1.600000000000000311 ) ) ;
#480=VERTEX_POINT ( 'NONE', #2766 ) ;
#482=EDGE_CURVE ( 'NONE', #954, #7060, #183, .T. ) ;
#487=CARTESIAN_POINT ( 'NONE',  ( 1.300000000000000044, 0.000000000000000000, 0.000000000000000000 ) ) ;
#500=VECTOR ( 'NONE', #5733, 1000.000000000000000 ) ;
#521=AXIS2_PLACEMENT_3D ( 'NONE', #6333, #6448, #1357 ) ;
#529=EDGE_CURVE ( 'NONE', #550, #1966, #3988, .T. ) ;
#532=AXIS2_PLACEMENT_3D ( 'NONE', #3087, #2422, #7488 ) ;
#543=EDGE_LOOP ( 'NONE', ( #6932, #3498, #8131, #4980, #1347 ) ) ;
#549=EDGE_CURVE ( 'NONE', #1740, #1171, #5269, .T. ) ;
#550=VERTEX_POINT ( 'NONE', #2722 ) ;
#572=EDGE_CURVE ( 'NONE', #954, #5018, #5312, .T. ) ;
#581=CARTESIAN_POINT ( 'NONE',  ( 10.71950000000001424, 0.000000000000000000, 0.000000000000000000 ) ) ;
#582=PRODUCT_DEFINITION_CONTEXT ( 'detailed design', #6602, 'design' ) ;
#586=FACE_OUTER_BOUND ( 'NONE', #8062, .T. ) ;
#591=VECTOR ( 'NONE', #2144, 1000.000000000000000 ) ;
#593=EDGE_CURVE ( 'NONE', #1776, #4324, #8006, .T. ) ;
#614=CARTESIAN_POINT ( 'NONE',  ( 2.039008344562727615, -1.214068345727601445E-18, 0.000000000000000000 ) ) ;
#618=AXIS2_PLACEMENT_3D ( 'NONE', #4404, #7425, #6266 ) ;
#633=ORIENTED_EDGE ( 'NONE', *, *, #8107, .F. ) ;
#645=VECTOR ( 'NONE', #1238, 1000.000000000000114 ) ;
#648=CARTESIAN_POINT ( 'NONE',  ( 3.000000000000002665, 0.000000000000000000, 0.000000000000000000 ) ) ;
#650=DIRECTION ( 'NONE',  ( 1.000000000000000000, 0.000000000000000000, 0.000000000000000000 ) ) ;
#651=DIRECTION ( 'NONE',  ( 0.000000000000000000, -0.8660254037844391517, -0.4999999999999992784 ) ) ;
#677=DIRECTION ( 'NONE',  ( -1.000000000000000000, -0.000000000000000000, -0.000000000000000000 ) ) ;
#680=VECTOR ( 'NONE', #7941, 1000.000000000000000 ) ;
#682=ORIENTED_EDGE ( 'NONE', *, *, #4050, .T. ) ;
#697=EDGE_CURVE ( 'NONE', #1740, #2560, #1589, .T. ) ;
#741=VERTEX_POINT ( 'NONE', #1345 ) ;
#758=DIRECTION ( 'NONE',  ( -1.000000000000000000, -0.000000000000000000, -0.000000000000000000 ) ) ;
#779=CIRCLE ( 'NONE', #1729, 1.280000000000000027 ) ;
#793=ORIENTED_EDGE ( 'NONE', *, *, #60, .F. ) ;
#804=CARTESIAN_POINT ( 'NONE',  ( 1.300000000000000044, -1.108512516844081475, 0.6400000000000016787 ) ) ;
#806=FACE_OUTER_BOUND ( 'NONE', #6674, .T. ) ;
#811=PLANE ( 'NONE',  #7019 ) ;
#815=AXIS2_PLACEMENT_3D ( 'NONE', #7607, #3697, #7563 ) ;
#827=ORIENTED_EDGE ( 'NONE', *, *, #3693, .F. ) ;
#830=DIRECTION ( 'NONE',  ( 1.000000000000000000, 0.000000000000000000, 0.000000000000000000 ) ) ;
#839=ADVANCED_FACE ( 'NONE', ( #1874 ), #6713, .F. ) ;
#846=ORIENTED_EDGE ( 'NONE', *, *, #2319, .T. ) ;
#852=ORIENTED_EDGE ( 'NONE', *, *, #1688, .T. ) ;
#871=EDGE_CURVE ( 'NONE', #5289, #7139, #5484, .T. ) ;
#878=DIRECTION ( 'NONE',  ( -1.000000000000000000, -0.000000000000000000, -0.000000000000000000 ) ) ;
#884=MECHANICAL_DESIGN_GEOMETRIC_PRESENTATION_REPRESENTATION('',(#8195),#7793);
#894=CARTESIAN_POINT ( 'NONE',  ( 10.71950000000001424, 1.836970198721030181E-16, -1.500000000000000222 ) ) ;
#896=CIRCLE ( 'NONE', #3029, 1.219500000000000028 ) ;
#899=DIRECTION ( 'NONE',  ( 0.000000000000000000, 0.000000000000000000, 1.000000000000000000 ) ) ;
#905=SURFACE_STYLE_FILL_AREA ( #5368 ) ;
#926=DIRECTION ( 'NONE',  ( 0.000000000000000000, 0.000000000000000000, -1.000000000000000000 ) ) ;
#954=VERTEX_POINT ( 'NONE', #1916 ) ;
#961=ORIENTED_EDGE ( 'NONE', *, *, #1230, .T. ) ;
#974=DIRECTION ( 'NONE',  ( -1.000000000000000000, -0.000000000000000000, -0.000000000000000000 ) ) ;
#978=CARTESIAN_POINT ( 'NONE',  ( 1.300000000000000044, -1.478016689125442706, 1.843143693225357538E-15 ) ) ;
#998=PRESENTATION_STYLE_ASSIGNMENT (( #5378 ) ) ;
#1017=CARTESIAN_POINT ( 'NONE',  ( 1.300000000000000044, 1.478016689125442484, -1.626303258728256651E-15 ) ) ;
#1021=DIRECTION ( 'NONE',  ( 1.000000000000000000, 0.000000000000000000, 0.000000000000000000 ) ) ;
#1028=EDGE_CURVE ( 'NONE', #7060, #5289, #1883, .T. ) ;
#1051=AXIS2_PLACEMENT_3D ( 'NONE', #2804, #3507, #5344 ) ;
#1054=DIRECTION ( 'NONE',  ( 1.000000000000000000, 0.000000000000000000, 0.000000000000000000 ) ) ;
#1078=FACE_OUTER_BOUND ( 'NONE', #5758, .T. ) ;
#1079=ADVANCED_FACE ( 'NONE', ( #4676, #2844 ), #4131, .T. ) ;
#1082=ORIENTED_EDGE ( 'NONE', *, *, #4413, .T. ) ;
#1095=ADVANCED_FACE ( 'NONE', ( #806 ), #7897, .T. ) ;
#1123=EDGE_LOOP ( 'NONE', ( #6954, #2857 ) ) ;
#1132=VERTEX_POINT ( 'NONE', #2100 ) ;
#1145=CARTESIAN_POINT ( 'NONE',  ( 0.1499999999999973577, 0.000000000000000000, 2.750000000000000000 ) ) ;
#1148=ORIENTED_EDGE ( 'NONE', *, *, #6993, .T. ) ;
#1171=VERTEX_POINT ( 'NONE', #178 ) ;
#1192=CARTESIAN_POINT ( 'NONE',  ( 3.000000000000000888, 0.000000000000000000, 0.000000000000000000 ) ) ;
#1214=ADVANCED_FACE ( 'NONE', ( #4883 ), #4003, .T. ) ;
#1218=CARTESIAN_POINT ( 'NONE',  ( 1.300000000000000044, 1.478016689125442484, -1.626303258728256651E-15 ) ) ;
#1227=FACE_OUTER_BOUND ( 'NONE', #4610, .T. ) ;
#1230=EDGE_CURVE ( 'NONE', #1132, #3745, #6871, .T. ) ;
#1232=DIRECTION ( 'NONE',  ( 0.000000000000000000, -0.4999999999999991118, 0.8660254037844391517 ) ) ;
#1233=CIRCLE ( 'NONE', #7066, 1.500000000000000222 ) ;
#1238=DIRECTION ( 'NONE',  ( 0.000000000000000000, 0.4999999999999991673, -0.8660254037844391517 ) ) ;
#1278=LINE ( 'NONE', #1439, #3861 ) ;
#1302=DIRECTION ( 'NONE',  ( 0.000000000000000000, 0.000000000000000000, 1.000000000000000000 ) ) ;
#1319=ORIENTED_EDGE ( 'NONE', *, *, #5004, .F. ) ;
#1325=VECTOR ( 'NONE', #254, 1000.000000000000000 ) ;
#1332=CIRCLE ( 'NONE', #2651, 1.280000000000000027 ) ;
#1336=FACE_OUTER_BOUND ( 'NONE', #6727, .T. ) ;
#1345=CARTESIAN_POINT ( 'NONE',  ( 0.000000000000000000, -1.478016689125442706, 1.843143693225357538E-15 ) ) ;
#1346=ORIENTED_EDGE ( 'NONE', *, *, #4496, .F. ) ;
#1347=ORIENTED_EDGE ( 'NONE', *, *, #6253, .T. ) ;
#1357=DIRECTION ( 'NONE',  ( 0.000000000000000000, 0.000000000000000000, 1.000000000000000000 ) ) ;
#1363=CIRCLE ( 'NONE', #815, 2.600000000000000089 ) ;
#1395=EDGE_LOOP ( 'NONE', ( #5774, #472, #852, #846 ) ) ;
#1396=DIRECTION ( 'NONE',  ( 0.000000000000000000, 0.000000000000000000, 1.000000000000000000 ) ) ;
#1404=DIRECTION ( 'NONE',  ( -1.000000000000000000, -0.000000000000000000, -0.000000000000000000 ) ) ;
#1411=CARTESIAN_POINT ( 'NONE',  ( 11.00000000000000355, 0.000000000000000000, 0.000000000000000000 ) ) ;
#1412=DIRECTION ( 'NONE',  ( 0.000000000000000000, -0.5000000000000009992, -0.8660254037844380415 ) ) ;
#1422=AXIS2_PLACEMENT_3D ( 'NONE', #1747, #5608, #1875 ) ;
#1439=CARTESIAN_POINT ( 'NONE',  ( 1.300000000000000044, 0.7390083445627193548, -1.280000000000000693 ) ) ;
#1457=ORIENTED_EDGE ( 'NONE', *, *, #4882, .T. ) ;
#1462=PLANE ( 'NONE',  #230 ) ;
#1477=AXIS2_PLACEMENT_3D ( 'NONE', #3055, #4799, #7985 ) ;
#1485=VERTEX_POINT ( 'NONE', #2875 ) ;
#1495=CARTESIAN_POINT ( 'NONE',  ( 1.300000000000000044, 1.478016689125442484, -1.626303258728256651E-15 ) ) ;
#1505=ORIENTED_EDGE ( 'NONE', *, *, #7848, .T. ) ;
#1511=SURFACE_STYLE_FILL_AREA ( #5296 ) ;
#1527=DIRECTION ( 'NONE',  ( -1.000000000000000000, -0.000000000000000000, -0.000000000000000000 ) ) ;
#1528=PLANE ( 'NONE',  #5581 ) ;
#1532=ORIENTED_EDGE ( 'NONE', *, *, #4413, .F. ) ;
#1555=VECTOR ( 'NONE', #5187, 1000.000000000000000 ) ;
#1572=CARTESIAN_POINT ( 'NONE',  ( -31.74999999999995737, 0.000000000000000000, 1.500000000000000222 ) ) ;
#1574=AXIS2_PLACEMENT_3D ( 'NONE', #7655, #6283, #1302 ) ;
#1576=CIRCLE ( 'NONE', #3308, 1.219500000000000028 ) ;
#1583=PLANE ( 'NONE',  #1844 ) ;
#1587=AXIS2_PLACEMENT_3D ( 'NONE', #3942, #5152, #6454 ) ;
#1589=CIRCLE ( 'NONE', #3192, 1.500000000000000222 ) ;
#1595=LINE ( 'NONE', #6561, #5721 ) ;
#1618=CARTESIAN_POINT ( 'NONE',  ( 3.099999999999998757, 0.000000000000000000, 0.000000000000000000 ) ) ;
#1621=CARTESIAN_POINT ( 'NONE',  ( 1.300000000000000044, 1.478016689125442484, -1.626303258728256651E-15 ) ) ;
#1637=CARTESIAN_POINT ( 'NONE',  ( 1.300000000000000044, 1.108512516844082141, 0.6399999999999991251 ) ) ;
#1646=DIRECTION ( 'NONE',  ( -1.000000000000000000, -0.000000000000000000, -0.000000000000000000 ) ) ;
#1648=ORIENTED_EDGE ( 'NONE', *, *, #84, .F. ) ;
#1649=ORIENTED_EDGE ( 'NONE', *, *, #3329, .T. ) ;
#1684=EDGE_CURVE ( 'NONE', #2291, #7441, #7253, .T. ) ;
#1688=EDGE_CURVE ( 'NONE', #2560, #7228, #6096, .T. ) ;
#1695=EDGE_LOOP ( 'NONE', ( #6559, #7035 ) ) ;
#1696=CIRCLE ( 'NONE', #7392, 2.750000000000000000 ) ;
#1705=DIRECTION ( 'NONE',  ( -1.000000000000000000, -0.000000000000000000, -0.000000000000000000 ) ) ;
#1721=CIRCLE ( 'NONE', #7023, 2.750000000000000000 ) ;
#1729=AXIS2_PLACEMENT_3D ( 'NONE', #3931, #5677, #1396 ) ;
#1730=CONICAL_SURFACE ( 'NONE', #1051, 1.219500000000000028, 0.7853981633974680410 ) ;
#1740=VERTEX_POINT ( 'NONE', #894 ) ;
#1747=CARTESIAN_POINT ( 'NONE',  ( 3.099999999999998757, 1.959434878635765477E-16, 1.600000000000000311 ) ) ;
#1776=VERTEX_POINT ( 'NONE', #5361 ) ;
#1784=EDGE_CURVE ( 'NONE', #2291, #480, #7179, .T. ) ;
#1790=DIRECTION ( 'NONE',  ( -1.000000000000000000, -0.000000000000000000, -0.000000000000000000 ) ) ;
#1826=EDGE_CURVE ( 'NONE', #1171, #7228, #4333, .T. ) ;
#1827=FACE_OUTER_BOUND ( 'NONE', #2336, .T. ) ;
#1844=AXIS2_PLACEMENT_3D ( 'NONE', #5980, #279, #7312 ) ;
#1849=CIRCLE ( 'NONE', #3840, 2.750000000000000000 ) ;
#1862=CARTESIAN_POINT ( 'NONE',  ( 11.00000000000000355, 1.219500000000000028, 0.000000000000000000 ) ) ;
#1874=FACE_OUTER_BOUND ( 'NONE', #2733, .T. ) ;
#1875=DIRECTION ( 'NONE',  ( 0.000000000000000000, 1.224646799147353207E-16, 1.000000000000000000 ) ) ;
#1883=CIRCLE ( 'NONE', #4931, 1.280000000000000027 ) ;
#1890=ORIENTED_EDGE ( 'NONE', *, *, #2741, .T. ) ;
#1916=CARTESIAN_POINT ( 'NONE',  ( 1.300000000000000044, -0.7390083445627200209, 1.280000000000001137 ) ) ;
#1918=EDGE_CURVE ( 'NONE', #7228, #1776, #7775, .T. ) ;
#1922=DIRECTION ( 'NONE',  ( 0.000000000000000000, 0.000000000000000000, -1.000000000000000000 ) ) ;
#1939=ORIENTED_EDGE ( 'NONE', *, *, #871, .F. ) ;
#1952=DIRECTION ( 'NONE',  ( 0.000000000000000000, 0.4999999999999992228, -0.8660254037844390407 ) ) ;
#1966=VERTEX_POINT ( 'NONE', #4898 ) ;
#1980=ADVANCED_FACE ( 'NONE', ( #2443, #1827 ), #6886, .T. ) ;
#1992=CARTESIAN_POINT ( 'NONE',  ( 11.00000000000000355, 0.000000000000000000, 0.000000000000000000 ) ) ;
#2004=CIRCLE ( 'NONE', #5308, 0.1499999999999999667 ) ;
#2024=ORIENTED_EDGE ( 'NONE', *, *, #593, .F. ) ;
#2048=ORIENTED_EDGE ( 'NONE', *, *, #3063, .F. ) ;
#2049=ORIENTED_EDGE ( 'NONE', *, *, #1688, .F. ) ;
#2053=( GEOMETRIC_REPRESENTATION_CONTEXT ( 3 ) GLOBAL_UNCERTAINTY_ASSIGNED_CONTEXT ( ( #2155 ) ) GLOBAL_UNIT_ASSIGNED_CONTEXT ( ( #7816, #5338, #2209 ) ) REPRESENTATION_CONTEXT ( 'NONE', 'WORKASPACE' ) );
#2058=DIRECTION ( 'NONE',  ( 0.000000000000000000, 0.000000000000000000, -1.000000000000000000 ) ) ;
#2060=CARTESIAN_POINT ( 'NONE',  ( 3.099999999999998757, 0.000000000000000000, 0.000000000000000000 ) ) ;
#2082=CARTESIAN_POINT ( 'NONE',  ( 1.300000000000000044, -0.7390083445627200209, 1.280000000000001137 ) ) ;
#2096=EDGE_CURVE ( 'NONE', #550, #2318, #4555, .T. ) ;
#2100=CARTESIAN_POINT ( 'NONE',  ( 0.000000000000000000, 0.7390083445627193548, -1.280000000000000693 ) ) ;
#2107=CARTESIAN_POINT ( 'NONE',  ( 1.300000000000000044, 1.478016689125442484, -1.626303258728256651E-15 ) ) ;
#2112=DIRECTION ( 'NONE',  ( -1.000000000000000000, -0.000000000000000000, -0.000000000000000000 ) ) ;
#2123=FACE_OUTER_BOUND ( 'NONE', #4286, .T. ) ;
#2127=ORIENTED_EDGE ( 'NONE', *, *, #5637, .T. ) ;
#2131=CARTESIAN_POINT ( 'NONE',  ( 3.099999999999998757, 0.000000000000000000, 0.000000000000000000 ) ) ;
#2132=FACE_OUTER_BOUND ( 'NONE', #228, .T. ) ;
#2144=DIRECTION ( 'NONE',  ( -1.000000000000000000, -0.000000000000000000, -0.000000000000000000 ) ) ;
#2146=LINE ( 'NONE', #5964, #355 ) ;
#2155=UNCERTAINTY_MEASURE_WITH_UNIT (LENGTH_MEASURE( 1.000000000000000082E-05 ), #7816, 'distance_accuracy_value', 'NONE');
#2158=CYLINDRICAL_SURFACE ( 'NONE', #5564, 2.750000000000000000 ) ;
#2209=( NAMED_UNIT ( * ) SI_UNIT ( $, .STERADIAN. ) SOLID_ANGLE_UNIT ( ) );
#2216=AXIS2_PLACEMENT_3D ( 'NONE', #5293, #5987, #4624 ) ;
#2218=ORIENTED_EDGE ( 'NONE', *, *, #7389, .F. ) ;
#2220=DIRECTION ( 'NONE',  ( 0.000000000000000000, -0.5000000000000013323, -0.8660254037844378194 ) ) ;
#2228=AXIS2_PLACEMENT_3D ( 'NONE', #487, #5406, #2984 ) ;
#2274=ADVANCED_FACE ( 'NONE', ( #4215 ), #3058, .F. ) ;
#2291=VERTEX_POINT ( 'NONE', #7366 ) ;
#2318=VERTEX_POINT ( 'NONE', #4936 ) ;
#2319=EDGE_CURVE ( 'NONE', #7228, #1171, #1233, .T. ) ;
#2321=ADVANCED_FACE ( 'NONE', ( #5072 ), #8196, .T. ) ;
#2336=EDGE_LOOP ( 'NONE', ( #1890, #3265 ) ) ;
#2339=FACE_OUTER_BOUND ( 'NONE', #1123, .T. ) ;
#2381=EDGE_LOOP ( 'NONE', ( #3082, #5166, #7491 ) ) ;
#2393=AXIS2_PLACEMENT_3D ( 'NONE', #7889, #4080, #5336 ) ;
#2397=VERTEX_POINT ( 'NONE', #268 ) ;
#2418=VERTEX_POINT ( 'NONE', #5892 ) ;
#2422=DIRECTION ( 'NONE',  ( -1.000000000000000000, -0.000000000000000000, -0.000000000000000000 ) ) ;
#2435=DIRECTION ( 'NONE',  ( 0.000000000000000000, 0.000000000000000000, -1.000000000000000000 ) ) ;
#2437=ORIENTED_EDGE ( 'NONE', *, *, #4578, .F. ) ;
#2443=FACE_BOUND ( 'NONE', #6635, .T. ) ;
#2458=EDGE_CURVE ( 'NONE', #5123, #1485, #4031, .T. ) ;
#2462=DIRECTION ( 'NONE',  ( 0.000000000000000000, 0.000000000000000000, -1.000000000000000000 ) ) ;
#2482=DIRECTION ( 'NONE',  ( 0.000000000000000000, 0.000000000000000000, -1.000000000000000000 ) ) ;
#2496=ADVANCED_FACE ( 'NONE', ( #3455 ), #4191, .F. ) ;
#2515=VECTOR ( 'NONE', #307, 1000.000000000000000 ) ;
#2524=AXIS2_PLACEMENT_3D ( 'NONE', #1862, #1054, #2965 ) ;
#2530=CARTESIAN_POINT ( 'NONE',  ( 3.000000000000002665, 0.000000000000000000, 0.000000000000000000 ) ) ;
#2538=CIRCLE ( 'NONE', #6083, 0.1000000000000000472 ) ;
#2560=VERTEX_POINT ( 'NONE', #5405 ) ;
#2565=LINE ( 'NONE', #6996, #5192 ) ;
#2575=FACE_OUTER_BOUND ( 'NONE', #3094, .T. ) ;
#2595=DIRECTION ( 'NONE',  ( 1.000000000000000000, 0.000000000000000000, 0.000000000000000000 ) ) ;
#2605=DIRECTION ( 'NONE',  ( 0.000000000000000000, -0.4999999999999992784, 0.8660254037844390407 ) ) ;
#2639=CONICAL_SURFACE ( 'NONE', #4494, 1.219500000000000028, 0.7853981633974680410 ) ;
#2651=AXIS2_PLACEMENT_3D ( 'NONE', #3854, #4466, #3770 ) ;
#2676=ORIENTED_EDGE ( 'NONE', *, *, #6190, .T. ) ;
#2677=CARTESIAN_POINT ( 'NONE',  ( 1.300000000000000044, -1.108512516844082141, -0.6399999999999991251 ) ) ;
#2686=CARTESIAN_POINT ( 'NONE',  ( 3.000000000000002665, 0.000000000000000000, 2.750000000000000000 ) ) ;
#2698=EDGE_CURVE ( 'NONE', #4304, #2418, #5342, .T. ) ;
#2722=CARTESIAN_POINT ( 'NONE',  ( 1.300000000000000044, 1.108512516844080364, -0.6400000000000017897 ) ) ;
#2733=EDGE_LOOP ( 'NONE', ( #2858, #5555, #7315 ) ) ;
#2734=VERTEX_POINT ( 'NONE', #614 ) ;
#2735=DIRECTION ( 'NONE',  ( 1.000000000000000000, 0.000000000000000000, 0.000000000000000000 ) ) ;
#2741=EDGE_CURVE ( 'NONE', #2418, #2397, #1363, .T. ) ;
#2747=ORIENTED_EDGE ( 'NONE', *, *, #529, .T. ) ;
#2766=CARTESIAN_POINT ( 'NONE',  ( 0.000000000000000000, 1.478016689125442484, -1.626303258728256651E-15 ) ) ;
#2772=CARTESIAN_POINT ( 'NONE',  ( 11.00000000000000355, 0.000000000000000000, 1.219500000000000028 ) ) ;
#2777=DIRECTION ( 'NONE',  ( -1.000000000000000000, -0.000000000000000000, -0.000000000000000000 ) ) ;
#2786=DIRECTION ( 'NONE',  ( 0.000000000000000000, 0.5000000000000013323, 0.8660254037844378194 ) ) ;
#2799=AXIS2_PLACEMENT_3D ( 'NONE', #6035, #878, #3984 ) ;
#2803=CARTESIAN_POINT ( 'NONE',  ( -31.74999999999995737, 0.000000000000000000, 2.750000000000000000 ) ) ;
#2804=CARTESIAN_POINT ( 'NONE',  ( 11.00000000000000355, 0.000000000000000000, 0.000000000000000000 ) ) ;
#2836=DIRECTION ( 'NONE',  ( -1.000000000000000000, -0.000000000000000000, -0.000000000000000000 ) ) ;
#2844=FACE_OUTER_BOUND ( 'NONE', #3641, .T. ) ;
#2857=ORIENTED_EDGE ( 'NONE', *, *, #6301, .F. ) ;
#2858=ORIENTED_EDGE ( 'NONE', *, *, #482, .F. ) ;
#2875=CARTESIAN_POINT ( 'NONE',  ( 1.300000000000000044, -0.7390083445627225744, -1.279999999999999138 ) ) ;
#2884=PRODUCT_DEFINITION ( 'UNKNOWN', '', #7087, #582 ) ;
#2888=DIRECTION ( 'NONE',  ( 0.000000000000000000, 0.000000000000000000, -1.000000000000000000 ) ) ;
#2889=COLOUR_RGB ( '', 0.72549020, 0.75294118, 0.79215686) ;
#2896=VECTOR ( 'NONE', #1705, 1000.000000000000000 ) ;
#2923=ORIENTED_EDGE ( 'NONE', *, *, #3134, .T. ) ;
#2939=DIRECTION ( 'NONE',  ( 0.000000000000000000, 1.000000000000000000, -1.026972870230479989E-15 ) ) ;
#2940=CARTESIAN_POINT ( 'NONE',  ( 1.300000000000000044, -0.7390083445627200209, 1.280000000000001137 ) ) ;
#2952=EDGE_LOOP ( 'NONE', ( #6085, #7583, #7151, #4345 ) ) ;
#2965=DIRECTION ( 'NONE',  ( 0.000000000000000000, 0.000000000000000000, -1.000000000000000000 ) ) ;
#2979=ORIENTED_EDGE ( 'NONE', *, *, #6953, .T. ) ;
#2984=DIRECTION ( 'NONE',  ( 0.000000000000000000, 0.000000000000000000, 1.000000000000000000 ) ) ;
#2985=ORIENTED_EDGE ( 'NONE', *, *, #2741, .F. ) ;
#2987=ORIENTED_EDGE ( 'NONE', *, *, #7974, .T. ) ;
#3012=DIRECTION ( 'NONE',  ( 0.000000000000000000, -1.000000000000000000, 0.000000000000000000 ) ) ;
#3025=AXIS2_PLACEMENT_3D ( 'NONE', #3739, #3781, #474 ) ;
#3026=LINE ( 'NONE', #7386, #2896 ) ;
#3029=AXIS2_PLACEMENT_3D ( 'NONE', #4377, #5137, #7619 ) ;
#3055=CARTESIAN_POINT ( 'NONE',  ( 0.1499999999999973577, 0.000000000000000000, 0.000000000000000000 ) ) ;
#3058=PLANE ( 'NONE',  #3764 ) ;
#3059=SHAPE_REPRESENTATION ( 'socket head cap screw_iso_ISO 4762 M3 x 8 - 8N', ( #1587 ), #3111 ) ;
#3063=EDGE_CURVE ( 'NONE', #7949, #5123, #2146, .T. ) ;
#3072=ORIENTED_EDGE ( 'NONE', *, *, #2096, .F. ) ;
#3082=ORIENTED_EDGE ( 'NONE', *, *, #1684, .F. ) ;
#3087=CARTESIAN_POINT ( 'NONE',  ( 0.1499999999999973577, 0.000000000000000000, 0.000000000000000000 ) ) ;
#3094=EDGE_LOOP ( 'NONE', ( #5982, #4998, #8076, #4419, #1505 ) ) ;
#3100=CARTESIAN_POINT ( 'NONE',  ( 1.300000000000000044, 1.478016689125442484, -1.626303258728256651E-15 ) ) ;
#3111=( GEOMETRIC_REPRESENTATION_CONTEXT ( 3 ) GLOBAL_UNCERTAINTY_ASSIGNED_CONTEXT ( ( #5895 ) ) GLOBAL_UNIT_ASSIGNED_CONTEXT ( ( #5909, #3418, #4741 ) ) REPRESENTATION_CONTEXT ( 'NONE', 'WORKASPACE' ) );
#3112=DIRECTION ( 'NONE',  ( 0.000000000000000000, 0.000000000000000000, -1.000000000000000000 ) ) ;
#3114=ORIENTED_EDGE ( 'NONE', *, *, #7795, .F. ) ;
#3123=EDGE_LOOP ( 'NONE', ( #4691, #3400, #3722, #1346, #6978 ) ) ;
#3134=EDGE_CURVE ( 'NONE', #1966, #2318, #6293, .T. ) ;
#3184=EDGE_LOOP ( 'NONE', ( #207, #1082, #4228, #198, #3410 ) ) ;
#3190=CARTESIAN_POINT ( 'NONE',  ( 1.300000000000000044, 0.7390083445627193548, -1.280000000000000693 ) ) ;
#3192=AXIS2_PLACEMENT_3D ( 'NONE', #581, #7024, #6278 ) ;
#3197=DIRECTION ( 'NONE',  ( 0.000000000000000000, -1.224646799147353207E-16, 1.000000000000000000 ) ) ;
#3198=LINE ( 'NONE', #6925, #500 ) ;
#3199=DIRECTION ( 'NONE',  ( -1.000000000000000000, -0.000000000000000000, -0.000000000000000000 ) ) ;
#3201=LINE ( 'NONE', #5117, #5301 ) ;
#3211=AXIS2_PLACEMENT_3D ( 'NONE', #3470, #7200, #926 ) ;
#3215=ORIENTED_EDGE ( 'NONE', *, *, #6190, .F. ) ;
#3220=PLANE ( 'NONE',  #5295 ) ;
#3225=ORIENTED_EDGE ( 'NONE', *, *, #2319, .F. ) ;
#3234=APPLICATION_CONTEXT ( 'automotive_design' ) ;
#3244=CARTESIAN_POINT ( 'NONE',  ( 1.300000000000000044, 1.478016689125442484, -1.626303258728256651E-15 ) ) ;
#3264=ADVANCED_FACE ( 'NONE', ( #1227 ), #6068, .F. ) ;
#3265=ORIENTED_EDGE ( 'NONE', *, *, #7559, .T. ) ;
#3283=ORIENTED_EDGE ( 'NONE', *, *, #3460, .T. ) ;
#3299=AXIS2_PLACEMENT_3D ( 'NONE', #3577, #7436, #4118 ) ;
#3307=CONICAL_SURFACE ( 'NONE', #1574, 1.280000000000000027, 1.047197551196593857 ) ;
#3308=AXIS2_PLACEMENT_3D ( 'NONE', #1992, #4523, #7049 ) ;
#3311=VECTOR ( 'NONE', #3692, 1000.000000000000000 ) ;
#3322=ADVANCED_FACE ( 'NONE', ( #5337 ), #5258, .T. ) ;
#3329=EDGE_CURVE ( 'NONE', #5320, #1740, #3378, .T. ) ;
#3336=ORIENTED_EDGE ( 'NONE', *, *, #7984, .T. ) ;
#3359=DIRECTION ( 'NONE',  ( 1.000000000000000000, 0.000000000000000000, 0.000000000000000000 ) ) ;
#3375=VECTOR ( 'NONE', #2220, 1000.000000000000227 ) ;
#3378=LINE ( 'NONE', #3465, #1555 ) ;
#3400=ORIENTED_EDGE ( 'NONE', *, *, #6998, .F. ) ;
#3410=ORIENTED_EDGE ( 'NONE', *, *, #2096, .T. ) ;
#3418=( NAMED_UNIT ( * ) PLANE_ANGLE_UNIT ( ) SI_UNIT ( $, .RADIAN. ) );
#3448=TOROIDAL_SURFACE ( 'NONE', #8081, 1.600000000000000311, 0.1000000000000000056 ) ;
#3455=FACE_OUTER_BOUND ( 'NONE', #3123, .T. ) ;
#3460=EDGE_CURVE ( 'NONE', #8184, #4662, #7976, .T. ) ;
#3461=ORIENTED_EDGE ( 'NONE', *, *, #2458, .F. ) ;
#3465=CARTESIAN_POINT ( 'NONE',  ( 11.00000000000000355, 1.493456771560197319E-16, -1.219500000000000028 ) ) ;
#3470=CARTESIAN_POINT ( 'NONE',  ( 3.000000000000000888, 2.750000000000000000, 0.000000000000000000 ) ) ;
#3482=AXIS2_PLACEMENT_3D ( 'NONE', #4434, #7594, #1232 ) ;
#3498=ORIENTED_EDGE ( 'NONE', *, *, #5637, .F. ) ;
#3507=DIRECTION ( 'NONE',  ( -1.000000000000000000, -0.000000000000000000, -0.000000000000000000 ) ) ;
#3511=CARTESIAN_POINT ( 'NONE',  ( 1.300000000000000044, 0.000000000000000000, 0.000000000000000000 ) ) ;
#3514=CARTESIAN_POINT ( 'NONE',  ( 3.000000000000000888, 0.000000000000000000, 0.000000000000000000 ) ) ;
#3564=DIRECTION ( 'NONE',  ( 0.000000000000000000, 0.000000000000000000, -1.000000000000000000 ) ) ;
#3573=VECTOR ( 'NONE', #1527, 1000.000000000000000 ) ;
#3577=CARTESIAN_POINT ( 'NONE',  ( 1.300000000000000044, -0.7390083445627200209, 1.280000000000001137 ) ) ;
#3583=EDGE_CURVE ( 'NONE', #7674, #5320, #896, .T. ) ;
#3607=DIRECTION ( 'NONE',  ( 0.000000000000000000, -1.026972870230479989E-15, -1.000000000000000000 ) ) ;
#3608=DIRECTION ( 'NONE',  ( 0.000000000000000000, 1.000000000000000000, -1.320393690296331133E-15 ) ) ;
#3609=ORIENTED_EDGE ( 'NONE', *, *, #7974, .F. ) ;
#3610=ADVANCED_FACE ( 'NONE', ( #6909 ), #3307, .F. ) ;
#3641=EDGE_LOOP ( 'NONE', ( #5113, #39 ) ) ;
#3662=EDGE_LOOP ( 'NONE', ( #7830, #1649, #7657, #827 ) ) ;
#3692=DIRECTION ( 'NONE',  ( 0.000000000000000000, -1.000000000000000000, 1.026972870230479989E-15 ) ) ;
#3693=EDGE_CURVE ( 'NONE', #7674, #2560, #5712, .T. ) ;
#3697=DIRECTION ( 'NONE',  ( -1.000000000000000000, -0.000000000000000000, -0.000000000000000000 ) ) ;
#3722=ORIENTED_EDGE ( 'NONE', *, *, #529, .F. ) ;
#3739=CARTESIAN_POINT ( 'NONE',  ( 1.300000000000000044, 0.000000000000000000, 0.000000000000000000 ) ) ;
#3740=DIRECTION ( 'NONE',  ( 0.000000000000000000, 0.000000000000000000, 1.000000000000000000 ) ) ;
#3745=VERTEX_POINT ( 'NONE', #4615 ) ;
#3764=AXIS2_PLACEMENT_3D ( 'NONE', #3100, #6127, #6789 ) ;
#3770=DIRECTION ( 'NONE',  ( 0.000000000000000000, 0.000000000000000000, 1.000000000000000000 ) ) ;
#3780=DIRECTION ( 'NONE',  ( 0.000000000000000000, 0.000000000000000000, -1.000000000000000000 ) ) ;
#3781=DIRECTION ( 'NONE',  ( -1.000000000000000000, -0.000000000000000000, -0.000000000000000000 ) ) ;
#3785=CARTESIAN_POINT ( 'NONE',  ( 1.300000000000000044, 0.000000000000000000, 0.000000000000000000 ) ) ;
#3791=DIRECTION ( 'NONE',  ( 0.000000000000000000, -1.000000000000000000, 0.000000000000000000 ) ) ;
#3840=AXIS2_PLACEMENT_3D ( 'NONE', #5812, #5274, #5241 ) ;
#3854=CARTESIAN_POINT ( 'NONE',  ( 1.300000000000000044, 0.000000000000000000, 0.000000000000000000 ) ) ;
#3861=VECTOR ( 'NONE', #1404, 1000.000000000000000 ) ;
#3888=ORIENTED_EDGE ( 'NONE', *, *, #1826, .T. ) ;
#3890=ADVANCED_FACE ( 'NONE', ( #1078 ), #1583, .T. ) ;
#3894=DIRECTION ( 'NONE',  ( 0.000000000000000000, -1.000000000000000000, 1.026972870230479989E-15 ) ) ;
#3895=ADVANCED_FACE ( 'NONE', ( #4782 ), #4909, .F. ) ;
#3931=CARTESIAN_POINT ( 'NONE',  ( 1.300000000000000044, 0.000000000000000000, 0.000000000000000000 ) ) ;
#3934=MANIFOLD_SOLID_BREP ( 'Hex', #7012 ) ;
#3940=CARTESIAN_POINT ( 'NONE',  ( 0.1499999999999973577, 3.184081677783118191E-16, -2.600000000000000089 ) ) ;
#3942=CARTESIAN_POINT ( 'NONE',  ( 0.000000000000000000, 0.000000000000000000, 0.000000000000000000 ) ) ;
#3980=CARTESIAN_POINT ( 'NONE',  ( 0.1499999999999973577, 3.367778697655221012E-16, -2.750000000000000000 ) ) ;
#3984=DIRECTION ( 'NONE',  ( 0.000000000000000000, 0.000000000000000000, 1.000000000000000000 ) ) ;
#3988=LINE ( 'NONE', #2107, #3375 ) ;
#3994=LINE ( 'NONE', #4489, #5448 ) ;
#4003=TOROIDAL_SURFACE ( 'NONE', #1477, 2.600000000000000089, 0.1499999999999999944 ) ;
#4031=LINE ( 'NONE', #6007, #6520 ) ;
#4050=EDGE_CURVE ( 'NONE', #5018, #741, #3994, .T. ) ;
#4056=DIRECTION ( 'NONE',  ( -1.000000000000000000, -0.000000000000000000, -0.000000000000000000 ) ) ;
#4080=DIRECTION ( 'NONE',  ( 1.000000000000000000, 0.000000000000000000, 0.000000000000000000 ) ) ;
#4086=CIRCLE ( 'NONE', #2228, 1.280000000000000027 ) ;
#4107=DIRECTION ( 'NONE',  ( 0.000000000000000000, -0.4999999999999992784, 0.8660254037844390407 ) ) ;
#4115=DIRECTION ( 'NONE',  ( 0.000000000000000000, 0.8660254037844379305, -0.5000000000000014433 ) ) ;
#4118=DIRECTION ( 'NONE',  ( 0.000000000000000000, -1.000000000000000000, 1.320393690296331133E-15 ) ) ;
#4123=ORIENTED_EDGE ( 'NONE', *, *, #4050, .F. ) ;
#4131=PLANE ( 'NONE',  #3211 ) ;
#4133=AXIS2_PLACEMENT_3D ( 'NONE', #5492, #4115, #2786 ) ;
#4135=ORIENTED_EDGE ( 'NONE', *, *, #6839, .F. ) ;
#4150=DIRECTION ( 'NONE',  ( 0.000000000000000000, 0.000000000000000000, -1.000000000000000000 ) ) ;
#4151=ADVANCED_FACE ( 'NONE', ( #5318 ), #1528, .F. ) ;
#4191=PLANE ( 'NONE',  #4133 ) ;
#4197=ORIENTED_EDGE ( 'NONE', *, *, #8107, .T. ) ;
#4215=FACE_OUTER_BOUND ( 'NONE', #5920, .T. ) ;
#4228=ORIENTED_EDGE ( 'NONE', *, *, #5618, .T. ) ;
#4248=PRODUCT_DEFINITION_SHAPE ( 'NONE', 'NONE',  #2884 ) ;
#4286=EDGE_LOOP ( 'NONE', ( #2048, #2218, #1319 ) ) ;
#4301=CARTESIAN_POINT ( 'NONE',  ( 3.099999999999998757, 0.000000000000000000, 0.000000000000000000 ) ) ;
#4304=VERTEX_POINT ( 'NONE', #1145 ) ;
#4324=VERTEX_POINT ( 'NONE', #5687 ) ;
#4333=CIRCLE ( 'NONE', #5267, 1.500000000000000222 ) ;
#4345=ORIENTED_EDGE ( 'NONE', *, *, #697, .F. ) ;
#4347=CARTESIAN_POINT ( 'NONE',  ( 0.000000000000000000, -1.478016689125442706, 1.843143693225357538E-15 ) ) ;
#4377=CARTESIAN_POINT ( 'NONE',  ( 11.00000000000000355, 0.000000000000000000, 0.000000000000000000 ) ) ;
#4381=EDGE_LOOP ( 'NONE', ( #961, #5333, #8090, #5000, #3 ) ) ;
#4388=CARTESIAN_POINT ( 'NONE',  ( 0.000000000000000000, -0.7390083445627200209, 1.280000000000001137 ) ) ;
#4401=DIRECTION ( 'NONE',  ( 0.000000000000000000, 0.000000000000000000, 1.000000000000000000 ) ) ;
#4404=CARTESIAN_POINT ( 'NONE',  ( 0.000000000000000000, 0.000000000000000000, 0.000000000000000000 ) ) ;
#4412=ADVANCED_FACE ( 'NONE', ( #2575 ), #7635, .T. ) ;
#4413=EDGE_CURVE ( 'NONE', #2734, #5289, #3201, .T. ) ;
#4419=ORIENTED_EDGE ( 'NONE', *, *, #7795, .T. ) ;
#4434=CARTESIAN_POINT ( 'NONE',  ( 1.300000000000000044, -1.478016689125442706, 1.843143693225357538E-15 ) ) ;
#4445=AXIS2_PLACEMENT_3D ( 'NONE', #3514, #974, #2888 ) ;
#4466=DIRECTION ( 'NONE',  ( -1.000000000000000000, -0.000000000000000000, -0.000000000000000000 ) ) ;
#4478=LINE ( 'NONE', #4347, #645 ) ;
#4480=DIRECTION ( 'NONE',  ( -0.5000000000000034417, 0.000000000000000000, 0.8660254037844367092 ) ) ;
#4489=CARTESIAN_POINT ( 'NONE',  ( 0.000000000000000000, -0.7390083445627200209, 1.280000000000001137 ) ) ;
#4494=AXIS2_PLACEMENT_3D ( 'NONE', #1411, #2112, #4645 ) ;
#4496=EDGE_CURVE ( 'NONE', #2291, #550, #4951, .T. ) ;
#4523=DIRECTION ( 'NONE',  ( -1.000000000000000000, -0.000000000000000000, -0.000000000000000000 ) ) ;
#4536=ADVANCED_FACE ( 'NONE', ( #5846 ), #7275, .F. ) ;
#4555=CIRCLE ( 'NONE', #5991, 1.280000000000000027 ) ;
#4578=EDGE_CURVE ( 'NONE', #7025, #4304, #4747, .T. ) ;
#4608=ORIENTED_EDGE ( 'NONE', *, *, #1826, .F. ) ;
#4610=EDGE_LOOP ( 'NONE', ( #6598, #4608, #4197, #2024 ) ) ;
#4615=CARTESIAN_POINT ( 'NONE',  ( 0.000000000000000000, -0.7390083445627225744, -1.279999999999999138 ) ) ;
#4624=DIRECTION ( 'NONE',  ( 0.000000000000000000, 0.000000000000000000, 1.000000000000000000 ) ) ;
#4631=AXIS2_PLACEMENT_3D ( 'NONE', #7475, #1790, #6177 ) ;
#4634=FACE_OUTER_BOUND ( 'NONE', #2952, .T. ) ;
#4645=DIRECTION ( 'NONE',  ( 0.000000000000000000, 0.000000000000000000, 1.000000000000000000 ) ) ;
#4650=DIRECTION ( 'NONE',  ( -1.000000000000000000, -0.000000000000000000, -0.000000000000000000 ) ) ;
#4662=VERTEX_POINT ( 'NONE', #3980 ) ;
#4676=FACE_BOUND ( 'NONE', #1695, .T. ) ;
#4691=ORIENTED_EDGE ( 'NONE', *, *, #60, .T. ) ;
#4710=DIRECTION ( 'NONE',  ( 0.000000000000000000, 0.000000000000000000, 1.000000000000000000 ) ) ;
#4716=CARTESIAN_POINT ( 'NONE',  ( 1.300000000000000044, -0.7390083445627200209, 1.280000000000001137 ) ) ;
#4741=( NAMED_UNIT ( * ) SI_UNIT ( $, .STERADIAN. ) SOLID_ANGLE_UNIT ( ) );
#4747=LINE ( 'NONE', #2803, #1325 ) ;
#4760=CARTESIAN_POINT ( 'NONE',  ( -31.74999999999995737, 1.836970198721030181E-16, -1.500000000000000222 ) ) ;
#4782=FACE_OUTER_BOUND ( 'NONE', #5222, .T. ) ;
#4799=DIRECTION ( 'NONE',  ( -1.000000000000000000, -0.000000000000000000, -0.000000000000000000 ) ) ;
#4822=FILL_AREA_STYLE_COLOUR ( '', #2889 ) ;
#4860=VECTOR ( 'NONE', #4107, 1000.000000000000000 ) ;
#4864=EDGE_CURVE ( 'NONE', #7441, #550, #779, .T. ) ;
#4882=EDGE_CURVE ( 'NONE', #2560, #1740, #7557, .T. ) ;
#4883=FACE_OUTER_BOUND ( 'NONE', #8059, .T. ) ;
#4897=DIRECTION ( 'NONE',  ( 1.000000000000000000, 0.000000000000000000, 0.000000000000000000 ) ) ;
#4898=CARTESIAN_POINT ( 'NONE',  ( 1.300000000000000044, 0.7390083445627193548, -1.280000000000000693 ) ) ;
#4899=ORIENTED_EDGE ( 'NONE', *, *, #7860, .F. ) ;
#4909=PLANE ( 'NONE',  #3299 ) ;
#4931=AXIS2_PLACEMENT_3D ( 'NONE', #3785, #5119, #6427 ) ;
#4936=CARTESIAN_POINT ( 'NONE',  ( 1.300000000000000044, -1.314525273895014473E-15, -1.280000000000000027 ) ) ;
#4951=LINE ( 'NONE', #6890, #7806 ) ;
#4980=ORIENTED_EDGE ( 'NONE', *, *, #2458, .T. ) ;
#4981=VECTOR ( 'NONE', #6622, 1000.000000000000114 ) ;
#4998=ORIENTED_EDGE ( 'NONE', *, *, #1784, .F. ) ;
#5000=ORIENTED_EDGE ( 'NONE', *, *, #3134, .F. ) ;
#5004=EDGE_CURVE ( 'NONE', #5123, #7060, #1332, .T. ) ;
#5018=VERTEX_POINT ( 'NONE', #4388 ) ;
#5031=ORIENTED_EDGE ( 'NONE', *, *, #6993, .F. ) ;
#5051=DIRECTION ( 'NONE',  ( 0.000000000000000000, 0.000000000000000000, 1.000000000000000000 ) ) ;
#5072=FACE_OUTER_BOUND ( 'NONE', #543, .T. ) ;
#5084=ADVANCED_FACE ( 'NONE', ( #5291 ), #3448, .F. ) ;
#5099=DIRECTION ( 'NONE',  ( -0.7071067811865335839, 0.000000000000000000, 0.7071067811865614505 ) ) ;
#5113=ORIENTED_EDGE ( 'NONE', *, *, #7984, .F. ) ;
#5117=CARTESIAN_POINT ( 'NONE',  ( 1.300000000000000044, 0.000000000000000000, 1.280000000000000027 ) ) ;
#5119=DIRECTION ( 'NONE',  ( -1.000000000000000000, -0.000000000000000000, -0.000000000000000000 ) ) ;
#5123=VERTEX_POINT ( 'NONE', #2677 ) ;
#5137=DIRECTION ( 'NONE',  ( -1.000000000000000000, -0.000000000000000000, -0.000000000000000000 ) ) ;
#5147=VECTOR ( 'NONE', #4650, 1000.000000000000000 ) ;
#5152=DIRECTION ( 'NONE',  ( 0.000000000000000000, 0.000000000000000000, 1.000000000000000000 ) ) ;
#5166=ORIENTED_EDGE ( 'NONE', *, *, #4496, .T. ) ;
#5187=DIRECTION ( 'NONE',  ( -0.7071067811865335839, 8.659560562355102956E-17, -0.7071067811865614505 ) ) ;
#5192=VECTOR ( 'NONE', #2605, 1000.000000000000000 ) ;
#5210=ORIENTED_EDGE ( 'NONE', *, *, #7389, .T. ) ;
#5222=EDGE_LOOP ( 'NONE', ( #6052, #7612, #1939, #1648, #7998 ) ) ;
#5240=COLOUR_RGB ( '', 0.72549020, 0.75294118, 0.79215686) ;
#5241=DIRECTION ( 'NONE',  ( 0.000000000000000000, 0.000000000000000000, 1.000000000000000000 ) ) ;
#5248=LINE ( 'NONE', #274, #7678 ) ;
#5258=CYLINDRICAL_SURFACE ( 'NONE', #2216, 1.500000000000000222 ) ;
#5267=AXIS2_PLACEMENT_3D ( 'NONE', #1618, #1021, #3564 ) ;
#5269=LINE ( 'NONE', #4760, #7629 ) ;
#5274=DIRECTION ( 'NONE',  ( 1.000000000000000000, 0.000000000000000000, 0.000000000000000000 ) ) ;
#5289=VERTEX_POINT ( 'NONE', #324 ) ;
#5291=FACE_OUTER_BOUND ( 'NONE', #7443, .T. ) ;
#5293=CARTESIAN_POINT ( 'NONE',  ( -31.74999999999995737, 0.000000000000000000, 0.000000000000000000 ) ) ;
#5295=AXIS2_PLACEMENT_3D ( 'NONE', #1218, #2595, #2462 ) ;
#5296=FILL_AREA_STYLE ('',( #5949 ) ) ;
#5301=VECTOR ( 'NONE', #4480, 999.9999999999998863 ) ;
#5308=AXIS2_PLACEMENT_3D ( 'NONE', #3940, #7124, #3197 ) ;
#5312=LINE ( 'NONE', #7831, #591 ) ;
#5313=TOROIDAL_SURFACE ( 'NONE', #532, 2.600000000000000089, 0.1499999999999999944 ) ;
#5318=FACE_OUTER_BOUND ( 'NONE', #4381, .T. ) ;
#5320=VERTEX_POINT ( 'NONE', #7617 ) ;
#5333=ORIENTED_EDGE ( 'NONE', *, *, #6253, .F. ) ;
#5336=DIRECTION ( 'NONE',  ( 0.000000000000000000, 0.000000000000000000, -1.000000000000000000 ) ) ;
#5337=FACE_OUTER_BOUND ( 'NONE', #1395, .T. ) ;
#5338=( NAMED_UNIT ( * ) PLANE_ANGLE_UNIT ( ) SI_UNIT ( $, .RADIAN. ) );
#5342=CIRCLE ( 'NONE', #7850, 0.1499999999999999667 ) ;
#5344=DIRECTION ( 'NONE',  ( 0.000000000000000000, 0.000000000000000000, 1.000000000000000000 ) ) ;
#5353=DIRECTION ( 'NONE',  ( 0.000000000000000000, 0.4999999999999991673, -0.8660254037844391517 ) ) ;
#5358=ADVANCED_FACE ( 'NONE', ( #8143 ), #3220, .F. ) ;
#5361=CARTESIAN_POINT ( 'NONE',  ( 3.000000000000000000, 1.959434878635765477E-16, 1.600000000000000311 ) ) ;
#5364=FACE_OUTER_BOUND ( 'NONE', #301, .T. ) ;
#5368=FILL_AREA_STYLE ('',( #4822 ) ) ;
#5376=DIRECTION ( 'NONE',  ( 0.000000000000000000, -0.5000000000000009992, -0.8660254037844380415 ) ) ;
#5378=SURFACE_STYLE_USAGE ( .BOTH. , #7891 ) ;
#5405=CARTESIAN_POINT ( 'NONE',  ( 10.71950000000001424, 0.000000000000000000, 1.500000000000000222 ) ) ;
#5406=DIRECTION ( 'NONE',  ( -1.000000000000000000, -0.000000000000000000, -0.000000000000000000 ) ) ;
#5407=PRESENTATION_STYLE_ASSIGNMENT (( #8005 ) ) ;
#5436=DIRECTION ( 'NONE',  ( 0.000000000000000000, -0.4999999999999992784, 0.8660254037844390407 ) ) ;
#5448=VECTOR ( 'NONE', #1412, 1000.000000000000114 ) ;
#5480=CARTESIAN_POINT ( 'NONE',  ( 0.000000000000000000, -0.7390083445627200209, 1.280000000000001137 ) ) ;
#5484=LINE ( 'NONE', #2940, #5840 ) ;
#5492=CARTESIAN_POINT ( 'NONE',  ( 1.300000000000000044, 1.478016689125442484, -1.626303258728256651E-15 ) ) ;
#5513=CARTESIAN_POINT ( 'NONE',  ( 0.000000000000000000, 0.7390083445627193548, -1.280000000000000693 ) ) ;
#5531=( LENGTH_UNIT ( ) NAMED_UNIT ( * ) SI_UNIT ( .MILLI., .METRE. ) );
#5555=ORIENTED_EDGE ( 'NONE', *, *, #84, .T. ) ;
#5564=AXIS2_PLACEMENT_3D ( 'NONE', #233, #7182, #899 ) ;
#5569=AXIS2_PLACEMENT_3D ( 'NONE', #28, #651, #1952 ) ;
#5571=CIRCLE ( 'NONE', #7553, 2.750000000000000000 ) ;
#5574=CARTESIAN_POINT ( 'NONE',  ( 0.1499999999999973577, 0.000000000000000000, 2.600000000000000089 ) ) ;
#5581=AXIS2_PLACEMENT_3D ( 'NONE', #435, #3607, #2939 ) ;
#5585=PRODUCT ( 'socket head cap screw_iso_ISO 4762 M3 x 8 - 8N', 'socket head cap screw_iso_ISO 4762 M3 x 8 - 8N', '', ( #6555 ) ) ;
#5605=CARTESIAN_POINT ( 'NONE',  ( 0.1499999999999973577, 0.000000000000000000, 0.000000000000000000 ) ) ;
#5608=DIRECTION ( 'NONE',  ( 0.000000000000000000, 1.000000000000000000, -1.224646799147353207E-16 ) ) ;
#5618=EDGE_CURVE ( 'NONE', #5289, #7441, #4086, .T. ) ;
#5637=EDGE_CURVE ( 'NONE', #7949, #741, #3026, .T. ) ;
#5677=DIRECTION ( 'NONE',  ( -1.000000000000000000, -0.000000000000000000, -0.000000000000000000 ) ) ;
#5687=CARTESIAN_POINT ( 'NONE',  ( 3.000000000000000000, 0.000000000000000000, -1.600000000000000311 ) ) ;
#5712=LINE ( 'NONE', #8, #7011 ) ;
#5721=VECTOR ( 'NONE', #5376, 1000.000000000000114 ) ;
#5733=DIRECTION ( 'NONE',  ( -1.000000000000000000, -0.000000000000000000, -0.000000000000000000 ) ) ;
#5758=EDGE_LOOP ( 'NONE', ( #4123, #6130, #1, #5210, #2127 ) ) ;
#5774=ORIENTED_EDGE ( 'NONE', *, *, #549, .F. ) ;
#5804=DIRECTION ( 'NONE',  ( 0.000000000000000000, 0.000000000000000000, 1.000000000000000000 ) ) ;
#5812=CARTESIAN_POINT ( 'NONE',  ( 0.1499999999999973577, 0.000000000000000000, 0.000000000000000000 ) ) ;
#5831=ORIENTED_EDGE ( 'NONE', *, *, #1028, .T. ) ;
#5840=VECTOR ( 'NONE', #3608, 1000.000000000000000 ) ;
#5846=FACE_OUTER_BOUND ( 'NONE', #3184, .T. ) ;
#5860=EDGE_CURVE ( 'NONE', #4304, #4662, #1849, .T. ) ;
#5892=CARTESIAN_POINT ( 'NONE',  ( 0.000000000000000000, 0.000000000000000000, 2.600000000000000089 ) ) ;
#5895=UNCERTAINTY_MEASURE_WITH_UNIT (LENGTH_MEASURE( 1.000000000000000082E-05 ), #5909, 'distance_accuracy_value', 'NONE');
#5898=DIRECTION ( 'NONE',  ( 0.000000000000000000, 1.000000000000000000, -1.320393690296331133E-15 ) ) ;
#5909=( LENGTH_UNIT ( ) NAMED_UNIT ( * ) SI_UNIT ( .MILLI., .METRE. ) );
#5916=ADVANCED_FACE ( 'NONE', ( #6509 ), #2639, .T. ) ;
#5920=EDGE_LOOP ( 'NONE', ( #7770, #3461, #3215 ) ) ;
#5949=FILL_AREA_STYLE_COLOUR ( '', #5240 ) ;
#5955=AXIS2_PLACEMENT_3D ( 'NONE', #7507, #4897, #3112 ) ;
#5964=CARTESIAN_POINT ( 'NONE',  ( 1.300000000000000044, -1.478016689125442706, 1.843143693225357538E-15 ) ) ;
#5980=CARTESIAN_POINT ( 'NONE',  ( 1.300000000000000044, -0.7390083445627200209, 1.280000000000001137 ) ) ;
#5982=ORIENTED_EDGE ( 'NONE', *, *, #7308, .F. ) ;
#5987=DIRECTION ( 'NONE',  ( -1.000000000000000000, -0.000000000000000000, -0.000000000000000000 ) ) ;
#5991=AXIS2_PLACEMENT_3D ( 'NONE', #3511, #1646, #4710 ) ;
#6007=CARTESIAN_POINT ( 'NONE',  ( 1.300000000000000044, -1.478016689125442706, 1.843143693225357538E-15 ) ) ;
#6035=CARTESIAN_POINT ( 'NONE',  ( -31.74999999999995737, 0.000000000000000000, 0.000000000000000000 ) ) ;
#6049=CARTESIAN_POINT ( 'NONE',  ( 1.300000000000000044, 1.478016689125442484, -1.626303258728256651E-15 ) ) ;
#6052=ORIENTED_EDGE ( 'NONE', *, *, #7860, .T. ) ;
#6068=TOROIDAL_SURFACE ( 'NONE', #8188, 1.600000000000000311, 0.1000000000000000056 ) ;
#6083=AXIS2_PLACEMENT_3D ( 'NONE', #475, #3012, #2482 ) ;
#6085=ORIENTED_EDGE ( 'NONE', *, *, #3329, .F. ) ;
#6096=LINE ( 'NONE', #1572, #473 ) ;
#6116=DIRECTION ( 'NONE',  ( -1.000000000000000000, -0.000000000000000000, -0.000000000000000000 ) ) ;
#6127=DIRECTION ( 'NONE',  ( 1.000000000000000000, 0.000000000000000000, 0.000000000000000000 ) ) ;
#6130=ORIENTED_EDGE ( 'NONE', *, *, #572, .F. ) ;
#6138=ORIENTED_EDGE ( 'NONE', *, *, #6189, .T. ) ;
#6152=MECHANICAL_DESIGN_GEOMETRIC_PRESENTATION_REPRESENTATION('',(#7745),#2053);
#6176=CARTESIAN_POINT ( 'NONE',  ( 1.300000000000000044, 0.7390083445627193548, -1.280000000000000693 ) ) ;
#6177=DIRECTION ( 'NONE',  ( 0.000000000000000000, 0.000000000000000000, 1.000000000000000000 ) ) ;
#6188=VERTEX_POINT ( 'NONE', #6212 ) ;
#6189=EDGE_CURVE ( 'NONE', #741, #3745, #4478, .T. ) ;
#6190=EDGE_CURVE ( 'NONE', #2318, #5123, #6595, .T. ) ;
#6212=CARTESIAN_POINT ( 'NONE',  ( 0.000000000000000000, 0.7390083445627224634, 1.279999999999999138 ) ) ;
#6214=VECTOR ( 'NONE', #2836, 1000.000000000000000 ) ;
#6253=EDGE_CURVE ( 'NONE', #1485, #3745, #3198, .T. ) ;
#6266=DIRECTION ( 'NONE',  ( -0.000000000000000000, 0.000000000000000000, 1.000000000000000000 ) ) ;
#6278=DIRECTION ( 'NONE',  ( 0.000000000000000000, 0.000000000000000000, 1.000000000000000000 ) ) ;
#6283=DIRECTION ( 'NONE',  ( -1.000000000000000000, -0.000000000000000000, -0.000000000000000000 ) ) ;
#6289=ORIENTED_EDGE ( 'NONE', *, *, #5004, .T. ) ;
#6293=LINE ( 'NONE', #3190, #7913 ) ;
#6301=EDGE_CURVE ( 'NONE', #5320, #7674, #1576, .T. ) ;
#6323=CARTESIAN_POINT ( 'NONE',  ( 1.300000000000000044, 1.567547902908612085E-16, -1.280000000000000027 ) ) ;
#6327=ORIENTED_EDGE ( 'NONE', *, *, #4578, .T. ) ;
#6333=CARTESIAN_POINT ( 'NONE',  ( 10.71950000000001424, 0.000000000000000000, 0.000000000000000000 ) ) ;
#6369=ORIENTED_EDGE ( 'NONE', *, *, #5860, .F. ) ;
#6406=ORIENTED_EDGE ( 'NONE', *, *, #1230, .F. ) ;
#6423=DIRECTION ( 'NONE',  ( 0.000000000000000000, -0.5000000000000013323, -0.8660254037844378194 ) ) ;
#6427=DIRECTION ( 'NONE',  ( 0.000000000000000000, 0.000000000000000000, 1.000000000000000000 ) ) ;
#6448=DIRECTION ( 'NONE',  ( -1.000000000000000000, -0.000000000000000000, -0.000000000000000000 ) ) ;
#6454=DIRECTION ( 'NONE',  ( 1.000000000000000000, 0.000000000000000000, 0.000000000000000000 ) ) ;
#6484=ORIENTED_EDGE ( 'NONE', *, *, #549, .T. ) ;
#6495=VECTOR ( 'NONE', #7835, 999.9999999999998863 ) ;
#6509=FACE_OUTER_BOUND ( 'NONE', #3662, .T. ) ;
#6520=VECTOR ( 'NONE', #6545, 1000.000000000000114 ) ;
#6526=DIRECTION ( 'NONE',  ( 1.000000000000000000, 0.000000000000000000, 0.000000000000000000 ) ) ;
#6545=DIRECTION ( 'NONE',  ( 0.000000000000000000, 0.4999999999999991673, -0.8660254037844391517 ) ) ;
#6555=PRODUCT_CONTEXT ( 'NONE', #3234, 'mechanical' ) ;
#6559=ORIENTED_EDGE ( 'NONE', *, *, #6839, .T. ) ;
#6561=CARTESIAN_POINT ( 'NONE',  ( 1.300000000000000044, -0.7390083445627200209, 1.280000000000001137 ) ) ;
#6574=VECTOR ( 'NONE', #5898, 1000.000000000000000 ) ;
#6595=CIRCLE ( 'NONE', #3025, 1.280000000000000027 ) ;
#6598=ORIENTED_EDGE ( 'NONE', *, *, #1918, .F. ) ;
#6602=APPLICATION_CONTEXT ( 'automotive_design' ) ;
#6622=DIRECTION ( 'NONE',  ( 0.000000000000000000, -0.5000000000000009992, -0.8660254037844380415 ) ) ;
#6635=EDGE_LOOP ( 'NONE', ( #7074, #4899, #682, #6138, #6406, #793 ) ) ;
#6663=ADVANCED_FACE ( 'NONE', ( #1336 ), #811, .F. ) ;
#6674=EDGE_LOOP ( 'NONE', ( #1457, #6484, #3888, #2049 ) ) ;
#6679=DIRECTION ( 'NONE',  ( 0.000000000000000000, -0.5000000000000013323, -0.8660254037844378194 ) ) ;
#6696=EDGE_LOOP ( 'NONE', ( #5031, #6369, #7103, #119 ) ) ;
#6700=CARTESIAN_POINT ( 'NONE',  ( 1.300000000000000044, 0.7390083445627224634, 1.279999999999999138 ) ) ;
#6713=PLANE ( 'NONE',  #5955 ) ;
#6727=EDGE_LOOP ( 'NONE', ( #7215, #3114, #269 ) ) ;
#6730=CARTESIAN_POINT ( 'NONE',  ( 0.000000000000000000, 0.000000000000000000, 0.000000000000000000 ) ) ;
#6789=DIRECTION ( 'NONE',  ( 0.000000000000000000, 0.000000000000000000, -1.000000000000000000 ) ) ;
#6793=DIRECTION ( 'NONE',  ( -1.000000000000000000, -0.000000000000000000, -0.000000000000000000 ) ) ;
#6839=EDGE_CURVE ( 'NONE', #4324, #1776, #7260, .T. ) ;
#6842=ORIENTED_EDGE ( 'NONE', *, *, #2698, .F. ) ;
#6871=LINE ( 'NONE', #5513, #680 ) ;
#6886=PLANE ( 'NONE',  #618 ) ;
#6890=CARTESIAN_POINT ( 'NONE',  ( 1.300000000000000044, 1.478016689125442484, -1.626303258728256651E-15 ) ) ;
#6907=DIRECTION ( 'NONE',  ( 0.000000000000000000, 0.000000000000000000, 1.000000000000000000 ) ) ;
#6909=FACE_OUTER_BOUND ( 'NONE', #7393, .T. ) ;
#6925=CARTESIAN_POINT ( 'NONE',  ( 1.300000000000000044, -0.7390083445627225744, -1.279999999999999138 ) ) ;
#6932=ORIENTED_EDGE ( 'NONE', *, *, #6189, .F. ) ;
#6953=EDGE_CURVE ( 'NONE', #8184, #7025, #1696, .T. ) ;
#6954=ORIENTED_EDGE ( 'NONE', *, *, #3583, .F. ) ;
#6978=ORIENTED_EDGE ( 'NONE', *, *, #1784, .T. ) ;
#6993=EDGE_CURVE ( 'NONE', #4662, #2397, #2004, .T. ) ;
#6996=CARTESIAN_POINT ( 'NONE',  ( 0.000000000000000000, 1.478016689125442484, -1.626303258728256651E-15 ) ) ;
#6998=EDGE_CURVE ( 'NONE', #1966, #1132, #1278, .T. ) ;
#7004=CARTESIAN_POINT ( 'NONE',  ( 3.000000000000002665, 3.367778697655221012E-16, -2.750000000000000000 ) ) ;
#7011=VECTOR ( 'NONE', #5099, 1000.000000000000000 ) ;
#7012=CLOSED_SHELL ( 'NONE', ( #3610, #1214, #5084, #5916, #1095, #7724, #1980, #96, #1079, #3322, #7122, #7252, #3264, #7543, #4412, #3895, #3890, #2321, #4151, #2496, #2274, #24, #839, #6663, #5358, #7409, #4536 ) ) ;
#7019=AXIS2_PLACEMENT_3D ( 'NONE', #3244, #3359, #7719 ) ;
#7023=AXIS2_PLACEMENT_3D ( 'NONE', #5605, #650, #4401 ) ;
#7024=DIRECTION ( 'NONE',  ( -1.000000000000000000, -0.000000000000000000, -0.000000000000000000 ) ) ;
#7025=VERTEX_POINT ( 'NONE', #2686 ) ;
#7029=CARTESIAN_POINT ( 'NONE',  ( -31.74999999999995737, 0.000000000000000000, 0.000000000000000000 ) ) ;
#7035=ORIENTED_EDGE ( 'NONE', *, *, #593, .T. ) ;
#7049=DIRECTION ( 'NONE',  ( 0.000000000000000000, 0.000000000000000000, 1.000000000000000000 ) ) ;
#7060=VERTEX_POINT ( 'NONE', #804 ) ;
#7066=AXIS2_PLACEMENT_3D ( 'NONE', #4301, #8117, #2435 ) ;
#7074=ORIENTED_EDGE ( 'NONE', *, *, #7308, .T. ) ;
#7087=PRODUCT_DEFINITION_FORMATION_WITH_SPECIFIED_SOURCE ( 'ANY', '', #5585, .NOT_KNOWN. ) ;
#7103=ORIENTED_EDGE ( 'NONE', *, *, #2698, .T. ) ;
#7122=ADVANCED_FACE ( 'NONE', ( #4634 ), #1730, .T. ) ;
#7124=DIRECTION ( 'NONE',  ( -0.000000000000000000, 1.000000000000000000, 1.224646799147353207E-16 ) ) ;
#7139=VERTEX_POINT ( 'NONE', #6700 ) ;
#7151=ORIENTED_EDGE ( 'NONE', *, *, #3693, .T. ) ;
#7154=PLANE ( 'NONE',  #2393 ) ;
#7156=DIRECTION ( 'NONE',  ( 0.000000000000000000, 0.000000000000000000, -1.000000000000000000 ) ) ;
#7179=LINE ( 'NONE', #6049, #5147 ) ;
#7182=DIRECTION ( 'NONE',  ( -1.000000000000000000, -0.000000000000000000, -0.000000000000000000 ) ) ;
#7200=DIRECTION ( 'NONE',  ( 1.000000000000000000, 0.000000000000000000, 0.000000000000000000 ) ) ;
#7215=ORIENTED_EDGE ( 'NONE', *, *, #871, .T. ) ;
#7228=VERTEX_POINT ( 'NONE', #8024 ) ;
#7247=LINE ( 'NONE', #5480, #2515 ) ;
#7252=ADVANCED_FACE ( 'NONE', ( #2339 ), #7535, .T. ) ;
#7253=LINE ( 'NONE', #1495, #4860 ) ;
#7260=CIRCLE ( 'NONE', #8192, 1.600000000000000311 ) ;
#7275=CONICAL_SURFACE ( 'NONE', #4631, 1.280000000000000027, 1.047197551196593857 ) ;
#7294=VECTOR ( 'NONE', #5436, 1000.000000000000000 ) ;
#7308=EDGE_CURVE ( 'NONE', #480, #6188, #2565, .T. ) ;
#7312=DIRECTION ( 'NONE',  ( 0.000000000000000000, 0.5000000000000009992, 0.8660254037844380415 ) ) ;
#7315=ORIENTED_EDGE ( 'NONE', *, *, #1028, .F. ) ;
#7335=CARTESIAN_POINT ( 'NONE',  ( 1.300000000000000044, 0.7390083445627224634, 1.279999999999999138 ) ) ;
#7366=CARTESIAN_POINT ( 'NONE',  ( 1.300000000000000044, 1.478016689125442484, -1.626303258728256651E-15 ) ) ;
#7386=CARTESIAN_POINT ( 'NONE',  ( 1.300000000000000044, -1.478016689125442706, 1.843143693225357538E-15 ) ) ;
#7389=EDGE_CURVE ( 'NONE', #7060, #7949, #1595, .T. ) ;
#7392=AXIS2_PLACEMENT_3D ( 'NONE', #648, #758, #5804 ) ;
#7393=EDGE_LOOP ( 'NONE', ( #1532, #260, #2676, #6289, #5831 ) ) ;
#7409=ADVANCED_FACE ( 'NONE', ( #2132 ), #7154, .F. ) ;
#7425=DIRECTION ( 'NONE',  ( -1.000000000000000000, 0.000000000000000000, -0.000000000000000000 ) ) ;
#7436=DIRECTION ( 'NONE',  ( -0.000000000000000000, 1.320393690296331133E-15, 1.000000000000000000 ) ) ;
#7441=VERTEX_POINT ( 'NONE', #1637 ) ;
#7443=EDGE_LOOP ( 'NONE', ( #3225, #13, #4135, #633 ) ) ;
#7475=CARTESIAN_POINT ( 'NONE',  ( 1.300000000000000044, 0.000000000000000000, 0.000000000000000000 ) ) ;
#7488=DIRECTION ( 'NONE',  ( 0.000000000000000000, 0.000000000000000000, 1.000000000000000000 ) ) ;
#7491=ORIENTED_EDGE ( 'NONE', *, *, #4864, .F. ) ;
#7507=CARTESIAN_POINT ( 'NONE',  ( 1.300000000000000044, 1.478016689125442484, -1.626303258728256651E-15 ) ) ;
#7535=PLANE ( 'NONE',  #2524 ) ;
#7543=ADVANCED_FACE ( 'NONE', ( #8015 ), #5313, .T. ) ;
#7553=AXIS2_PLACEMENT_3D ( 'NONE', #2530, #3199, #3740 ) ;
#7557=CIRCLE ( 'NONE', #521, 1.500000000000000222 ) ;
#7559=EDGE_CURVE ( 'NONE', #2397, #2418, #8091, .T. ) ;
#7563=DIRECTION ( 'NONE',  ( 0.000000000000000000, 0.000000000000000000, 1.000000000000000000 ) ) ;
#7583=ORIENTED_EDGE ( 'NONE', *, *, #6301, .T. ) ;
#7594=DIRECTION ( 'NONE',  ( -0.000000000000000000, 0.8660254037844391517, 0.4999999999999991118 ) ) ;
#7607=CARTESIAN_POINT ( 'NONE',  ( 0.000000000000000000, 0.000000000000000000, 0.000000000000000000 ) ) ;
#7612=ORIENTED_EDGE ( 'NONE', *, *, #7848, .F. ) ;
#7617=CARTESIAN_POINT ( 'NONE',  ( 11.00000000000000355, 1.665213485140613626E-16, -1.219500000000000028 ) ) ;
#7619=DIRECTION ( 'NONE',  ( 0.000000000000000000, 0.000000000000000000, 1.000000000000000000 ) ) ;
#7629=VECTOR ( 'NONE', #4056, 1000.000000000000000 ) ;
#7635=PLANE ( 'NONE',  #5569 ) ;
#7654=CYLINDRICAL_SURFACE ( 'NONE', #8205, 2.750000000000000000 ) ;
#7655=CARTESIAN_POINT ( 'NONE',  ( 1.300000000000000044, 0.000000000000000000, 0.000000000000000000 ) ) ;
#7657=ORIENTED_EDGE ( 'NONE', *, *, #4882, .F. ) ;
#7666=EDGE_CURVE ( 'NONE', #2734, #2318, #8181, .T. ) ;
#7674=VERTEX_POINT ( 'NONE', #2772 ) ;
#7678=VECTOR ( 'NONE', #6679, 1000.000000000000227 ) ;
#7719=DIRECTION ( 'NONE',  ( 0.000000000000000000, 0.000000000000000000, -1.000000000000000000 ) ) ;
#7724=ADVANCED_FACE ( 'NONE', ( #586 ), #7654, .T. ) ;
#7745=STYLED_ITEM ( 'NONE', ( #998 ), #9 ) ;
#7760=LINE ( 'NONE', #2082, #6574 ) ;
#7770=ORIENTED_EDGE ( 'NONE', *, *, #148, .T. ) ;
#7775=CIRCLE ( 'NONE', #1422, 0.1000000000000000472 ) ;
#7793=( GEOMETRIC_REPRESENTATION_CONTEXT ( 3 ) GLOBAL_UNCERTAINTY_ASSIGNED_CONTEXT ( ( #383 ) ) GLOBAL_UNIT_ASSIGNED_CONTEXT ( ( #5531, #7919, #409 ) ) REPRESENTATION_CONTEXT ( 'NONE', 'WORKASPACE' ) );
#7795=EDGE_CURVE ( 'NONE', #7441, #7139, #7956, .T. ) ;
#7806=VECTOR ( 'NONE', #6423, 1000.000000000000227 ) ;
#7816=( LENGTH_UNIT ( ) NAMED_UNIT ( * ) SI_UNIT ( .MILLI., .METRE. ) );
#7830=ORIENTED_EDGE ( 'NONE', *, *, #3583, .T. ) ;
#7831=CARTESIAN_POINT ( 'NONE',  ( 1.300000000000000044, -0.7390083445627200209, 1.280000000000001137 ) ) ;
#7835=DIRECTION ( 'NONE',  ( -0.5000000000000034417, 1.060575238724904696E-16, -0.8660254037844367092 ) ) ;
#7848=EDGE_CURVE ( 'NONE', #7139, #6188, #433, .T. ) ;
#7850=AXIS2_PLACEMENT_3D ( 'NONE', #5574, #3791, #1922 ) ;
#7860=EDGE_CURVE ( 'NONE', #5018, #6188, #7247, .T. ) ;
#7889=CARTESIAN_POINT ( 'NONE',  ( 1.300000000000000044, 1.478016689125442484, -1.626303258728256651E-15 ) ) ;
#7891=SURFACE_SIDE_STYLE ('',( #1511 ) ) ;
#7897=CYLINDRICAL_SURFACE ( 'NONE', #2799, 1.500000000000000222 ) ;
#7913=VECTOR ( 'NONE', #3894, 1000.000000000000000 ) ;
#7919=( NAMED_UNIT ( * ) PLANE_ANGLE_UNIT ( ) SI_UNIT ( $, .RADIAN. ) );
#7941=DIRECTION ( 'NONE',  ( 0.000000000000000000, -1.000000000000000000, 1.026972870230479989E-15 ) ) ;
#7949=VERTEX_POINT ( 'NONE', #978 ) ;
#7956=LINE ( 'NONE', #1017, #7294 ) ;
#7974=EDGE_CURVE ( 'NONE', #4662, #4304, #1721, .T. ) ;
#7976=LINE ( 'NONE', #415, #6214 ) ;
#7984=EDGE_CURVE ( 'NONE', #7025, #8184, #5571, .T. ) ;
#7985=DIRECTION ( 'NONE',  ( 0.000000000000000000, 0.000000000000000000, 1.000000000000000000 ) ) ;
#7998=ORIENTED_EDGE ( 'NONE', *, *, #572, .T. ) ;
#8001=LINE ( 'NONE', #6176, #3311 ) ;
#8005=SURFACE_STYLE_USAGE ( .BOTH. , #320 ) ;
#8006=CIRCLE ( 'NONE', #4445, 1.600000000000000311 ) ;
#8015=FACE_OUTER_BOUND ( 'NONE', #6696, .T. ) ;
#8024=CARTESIAN_POINT ( 'NONE',  ( 3.099999999999998757, 0.000000000000000000, 1.500000000000000222 ) ) ;
#8059=EDGE_LOOP ( 'NONE', ( #3609, #1148, #2985, #6842 ) ) ;
#8062=EDGE_LOOP ( 'NONE', ( #3336, #3283, #2987, #2437 ) ) ;
#8076=ORIENTED_EDGE ( 'NONE', *, *, #1684, .T. ) ;
#8081=AXIS2_PLACEMENT_3D ( 'NONE', #2131, #830, #2058 ) ;
#8090=ORIENTED_EDGE ( 'NONE', *, *, #148, .F. ) ;
#8091=CIRCLE ( 'NONE', #384, 2.600000000000000089 ) ;
#8103=ORIENTED_EDGE ( 'NONE', *, *, #5860, .T. ) ;
#8107=EDGE_CURVE ( 'NONE', #1171, #4324, #2538, .T. ) ;
#8117=DIRECTION ( 'NONE',  ( 1.000000000000000000, 0.000000000000000000, 0.000000000000000000 ) ) ;
#8131=ORIENTED_EDGE ( 'NONE', *, *, #3063, .T. ) ;
#8143=FACE_OUTER_BOUND ( 'NONE', #2381, .T. ) ;
#8181=LINE ( 'NONE', #6323, #6495 ) ;
#8184=VERTEX_POINT ( 'NONE', #7004 ) ;
#8188=AXIS2_PLACEMENT_3D ( 'NONE', #2060, #6526, #7156 ) ;
#8192=AXIS2_PLACEMENT_3D ( 'NONE', #1192, #6793, #3780 ) ;
#8195=STYLED_ITEM ( 'NONE', ( #5407 ), #3934 ) ;
#8196=PLANE ( 'NONE',  #3482 ) ;
#8205=AXIS2_PLACEMENT_3D ( 'NONE', #7029, #677, #5051 ) ;
ENDSEC;
END-ISO-10303-21;
